ISO-10303-21;
HEADER;
/* Generated by software containing ST-Developer
 * from STEP Tools, Inc. (www.steptools.com) 
 */

FILE_DESCRIPTION(
/* description */ ('PAT-015'),
/* implementation_level */ '2;1');

FILE_NAME(
/* name */ 'Adjusting screw.step',
/* time_stamp */ '2026-10-29T16:03:43-07:00',
/* author */ (''),
/* organization */ (''),
/* preprocessor_version */ 'ST-DEVELOPER v20.2',
/* originating_system */ 'Autodesk Translation Framework v15.17.0.0',
/* authorisation */ '');

FILE_SCHEMA (('AUTOMOTIVE_DESIGN { 1 0 10303 214 3 1 1 }'));
ENDSEC;

DATA;
#10=MECHANICAL_DESIGN_GEOMETRIC_PRESENTATION_REPRESENTATION('',(#246),#10266);
#198=SHAPE_REPRESENTATION_RELATIONSHIP('SRR','None',#10369,#221);
#221=ADVANCED_BREP_SHAPE_REPRESENTATION('',(#271),#10257);
#246=STYLED_ITEM('',(#10554),#271);
#271=MANIFOLD_SOLID_BREP('Body1',#4705);
#518=PLANE('',#5396);
#519=PLANE('',#5397);
#775=FACE_OUTER_BOUND('',#1173,.T.);
#776=FACE_OUTER_BOUND('',#1174,.T.);
#777=FACE_OUTER_BOUND('',#1175,.T.);
#1173=EDGE_LOOP('',(#3981,#3982,#3983,#3984));
#1174=EDGE_LOOP('',(#3985));
#1175=EDGE_LOOP('',(#3986));
#1504=LINE('',#9770,#1784);
#1784=VECTOR('',#6587,0.4);
#2073=CIRCLE('',#5394,0.4);
#2074=CIRCLE('',#5395,0.4);
#2407=VERTEX_POINT('',#9767);
#2408=VERTEX_POINT('',#9769);
#2946=EDGE_CURVE('',#2407,#2407,#2073,.T.);
#2947=EDGE_CURVE('',#2407,#2408,#1504,.T.);
#2948=EDGE_CURVE('',#2408,#2408,#2074,.T.);
#3981=ORIENTED_EDGE('',*,*,#2946,.F.);
#3982=ORIENTED_EDGE('',*,*,#2947,.T.);
#3983=ORIENTED_EDGE('',*,*,#2948,.T.);
#3984=ORIENTED_EDGE('',*,*,#2947,.F.);
#3985=ORIENTED_EDGE('',*,*,#2946,.T.);
#3986=ORIENTED_EDGE('',*,*,#2948,.F.);
#4393=CYLINDRICAL_SURFACE('',#5393,0.4);
#4610=ADVANCED_FACE('',(#775),#4393,.T.);
#4611=ADVANCED_FACE('',(#776),#518,.T.);
#4612=ADVANCED_FACE('',(#777),#519,.F.);
#4705=CLOSED_SHELL('',(#4610,#4611,#4612));
#5392=AXIS2_PLACEMENT_3D('',#9765,#6581,#6582);
#5393=AXIS2_PLACEMENT_3D('',#9766,#6583,#6584);
#5394=AXIS2_PLACEMENT_3D('',#9768,#6585,#6586);
#5395=AXIS2_PLACEMENT_3D('',#9771,#6588,#6589);
#5396=AXIS2_PLACEMENT_3D('',#9772,#6590,#6591);
#5397=AXIS2_PLACEMENT_3D('',#9773,#6592,#6593);
#6581=DIRECTION('axis',(0.,0.,1.));
#6582=DIRECTION('refdir',(1.,0.,0.));
#6583=DIRECTION('center_axis',(0.,0.,1.));
#6584=DIRECTION('ref_axis',(1.,0.,0.));
#6585=DIRECTION('center_axis',(0.,0.,1.));
#6586=DIRECTION('ref_axis',(1.,0.,0.));
#6587=DIRECTION('',(0.,0.,-1.));
#6588=DIRECTION('center_axis',(0.,0.,1.));
#6589=DIRECTION('ref_axis',(1.,0.,0.));
#6590=DIRECTION('center_axis',(0.,0.,1.));
#6591=DIRECTION('ref_axis',(1.,0.,0.));
#6592=DIRECTION('center_axis',(0.,0.,1.));
#6593=DIRECTION('ref_axis',(1.,0.,0.));
#9765=CARTESIAN_POINT('',(0.,0.,0.));
#9766=CARTESIAN_POINT('Origin',(0.,0.,8.));
#9767=CARTESIAN_POINT('',(-0.4,-4.89858719658941E-17,11.));
#9768=CARTESIAN_POINT('Origin',(0.,0.,11.));
#9769=CARTESIAN_POINT('',(-0.4,-4.89858719658941E-17,8.));
#9770=CARTESIAN_POINT('',(-0.4,-4.89858719658941E-17,8.));
#9771=CARTESIAN_POINT('Origin',(0.,0.,8.));
#9772=CARTESIAN_POINT('Origin',(0.,0.,11.));
#9773=CARTESIAN_POINT('Origin',(0.,0.,8.));
#10232=UNCERTAINTY_MEASURE_WITH_UNIT(LENGTH_MEASURE(0.001),#10267,
'DISTANCE_ACCURACY_VALUE',
'Maximum model space distance between geometric entities at asserted c
onnectivities');
#10241=UNCERTAINTY_MEASURE_WITH_UNIT(LENGTH_MEASURE(0.001),#10267,
'DISTANCE_ACCURACY_VALUE',
'Maximum model space distance between geometric entities at asserted c
onnectivities');
#10257=(
GEOMETRIC_REPRESENTATION_CONTEXT(3)
GLOBAL_UNCERTAINTY_ASSIGNED_CONTEXT((#10232))
GLOBAL_UNIT_ASSIGNED_CONTEXT((#10267,#10269,#10270))
REPRESENTATION_CONTEXT('','3D')
);
#10266=(
GEOMETRIC_REPRESENTATION_CONTEXT(3)
GLOBAL_UNCERTAINTY_ASSIGNED_CONTEXT((#10241))
GLOBAL_UNIT_ASSIGNED_CONTEXT((#10267,#10269,#10270))
REPRESENTATION_CONTEXT('','3D')
);
#10267=(
LENGTH_UNIT()
NAMED_UNIT(*)
SI_UNIT(.CENTI.,.METRE.)
);
#10269=(
NAMED_UNIT(*)
PLANE_ANGLE_UNIT()
SI_UNIT($,.RADIAN.)
);
#10270=(
NAMED_UNIT(*)
SI_UNIT($,.STERADIAN.)
SOLID_ANGLE_UNIT()
);
#10286=SHAPE_DEFINITION_REPRESENTATION(#10310,#10369);
#10310=PRODUCT_DEFINITION_SHAPE('',$,#10394);
#10369=SHAPE_REPRESENTATION('',(#5392),#10257);
#10378=PRODUCT_DEFINITION_CONTEXT('part definition',#10452,'design');
#10394=PRODUCT_DEFINITION('Adjusting screw','Adjusting screw',
#10418,#10378);
#10418=PRODUCT_DEFINITION_FORMATION('',$,#10469);
#10452=APPLICATION_CONTEXT(
'Core Data for Automotive Mechanical Design Process');
#10453=PRODUCT_CONTEXT('part definition',#10452,'mechanical');
#10469=PRODUCT('Adjusting screw','Adjusting screw',
'Adjusting screw',(#10453));
#10548=COLOUR_RGB('Black',0.12,0.14,0.17);
#10549=FILL_AREA_STYLE_COLOUR('',#10548);
#10550=FILL_AREA_STYLE('',(#10549));
#10551=SURFACE_STYLE_FILL_AREA(#10550);
#10552=SURFACE_SIDE_STYLE('',(#10551));
#10553=SURFACE_STYLE_USAGE(.BOTH.,#10552);
#10554=PRESENTATION_STYLE_ASSIGNMENT((#10553));
ENDSEC;
END-ISO-10303-21;
